ISO-10303-21;
HEADER;
/* Generated by software containing ST-Developer
 * from STEP Tools, Inc. (www.steptools.com) 
 */

FILE_DESCRIPTION(
/* description */ ('Grid plate located blocks and clamp'),
/* implementation_level */ '2;1');

FILE_NAME(
/* name */ 'Cap Screw - M6x25.step',
/* time_stamp */ '2026-10-29T15:43:47-07:00',
/* author */ (''),
/* organization */ (''),
/* preprocessor_version */ 'ST-DEVELOPER v20.2',
/* originating_system */ 'Autodesk Translation Framework v15.17.0.0',
/* authorisation */ '');

FILE_SCHEMA (('AUTOMOTIVE_DESIGN { 1 0 10303 214 3 1 1 }'));
ENDSEC;

DATA;
#10=MECHANICAL_DESIGN_GEOMETRIC_PRESENTATION_REPRESENTATION('',(#171),#5702);
#127=ORIENTED_CLOSED_SHELL('',*,#3267,.F.);
#129=CONICAL_SURFACE('',#3568,0.475,0.785398163397449);
#130=CONICAL_SURFACE('',#3572,0.485,0.785398163397448);
#131=CONICAL_SURFACE('',#3576,0.31,0.463647609000806);
#132=CONICAL_SURFACE('',#3580,0.27,0.785398163397448);
#138=BREP_WITH_VOIDS('Body1',#3266,(#127));
#145=SHAPE_REPRESENTATION_RELATIONSHIP('SRR','None',#5763,#157);
#157=ADVANCED_BREP_SHAPE_REPRESENTATION('',(#138),#5693);
#171=STYLED_ITEM('',(#5904),#138);
#249=FACE_BOUND('',#789,.T.);
#330=CIRCLE('',#3567,0.45);
#331=CIRCLE('',#3569,0.5);
#332=CIRCLE('',#3571,0.5);
#333=CIRCLE('',#3573,0.47);
#334=CIRCLE('',#3575,0.32);
#335=CIRCLE('',#3577,0.2942);
#336=CIRCLE('',#3579,0.2942);
#337=CIRCLE('',#3581,0.24);
#428=CYLINDRICAL_SURFACE('',#3570,0.5);
#429=CYLINDRICAL_SURFACE('',#3578,0.2942);
#544=FACE_OUTER_BOUND('',#784,.T.);
#545=FACE_OUTER_BOUND('',#785,.T.);
#546=FACE_OUTER_BOUND('',#786,.T.);
#547=FACE_OUTER_BOUND('',#787,.T.);
#548=FACE_OUTER_BOUND('',#788,.T.);
#549=FACE_OUTER_BOUND('',#790,.T.);
#550=FACE_OUTER_BOUND('',#791,.T.);
#551=FACE_OUTER_BOUND('',#792,.T.);
#552=FACE_OUTER_BOUND('',#793,.T.);
#553=FACE_OUTER_BOUND('',#794,.T.);
#554=FACE_OUTER_BOUND('',#795,.T.);
#555=FACE_OUTER_BOUND('',#796,.T.);
#556=FACE_OUTER_BOUND('',#797,.T.);
#557=FACE_OUTER_BOUND('',#798,.T.);
#558=FACE_OUTER_BOUND('',#799,.T.);
#559=FACE_OUTER_BOUND('',#800,.T.);
#560=FACE_OUTER_BOUND('',#801,.T.);
#784=EDGE_LOOP('',(#2568));
#785=EDGE_LOOP('',(#2569,#2570,#2571,#2572));
#786=EDGE_LOOP('',(#2573,#2574,#2575,#2576));
#787=EDGE_LOOP('',(#2577,#2578,#2579,#2580));
#788=EDGE_LOOP('',(#2581));
#789=EDGE_LOOP('',(#2582));
#790=EDGE_LOOP('',(#2583,#2584,#2585,#2586));
#791=EDGE_LOOP('',(#2587,#2588,#2589,#2590));
#792=EDGE_LOOP('',(#2591,#2592,#2593,#2594));
#793=EDGE_LOOP('',(#2595));
#794=EDGE_LOOP('',(#2596,#2597,#2598,#2599));
#795=EDGE_LOOP('',(#2600,#2601,#2602,#2603));
#796=EDGE_LOOP('',(#2604,#2605,#2606,#2607));
#797=EDGE_LOOP('',(#2608,#2609,#2610,#2611));
#798=EDGE_LOOP('',(#2612,#2613,#2614,#2615));
#799=EDGE_LOOP('',(#2616,#2617,#2618,#2619));
#800=EDGE_LOOP('',(#2620,#2621,#2622,#2623,#2624,#2625));
#801=EDGE_LOOP('',(#2626,#2627,#2628,#2629,#2630,#2631));
#1053=LINE('',#5200,#1326);
#1054=LINE('',#5204,#1327);
#1055=LINE('',#5208,#1328);
#1056=LINE('',#5215,#1329);
#1057=LINE('',#5219,#1330);
#1058=LINE('',#5223,#1331);
#1059=LINE('',#5228,#1332);
#1060=LINE('',#5230,#1333);
#1061=LINE('',#5232,#1334);
#1062=LINE('',#5233,#1335);
#1063=LINE('',#5236,#1336);
#1064=LINE('',#5238,#1337);
#1065=LINE('',#5239,#1338);
#1066=LINE('',#5242,#1339);
#1067=LINE('',#5244,#1340);
#1068=LINE('',#5245,#1341);
#1069=LINE('',#5248,#1342);
#1070=LINE('',#5250,#1343);
#1071=LINE('',#5251,#1344);
#1072=LINE('',#5254,#1345);
#1073=LINE('',#5256,#1346);
#1074=LINE('',#5257,#1347);
#1075=LINE('',#5259,#1348);
#1076=LINE('',#5260,#1349);
#1326=VECTOR('',#4237,0.475);
#1327=VECTOR('',#4242,0.5);
#1328=VECTOR('',#4247,0.485);
#1329=VECTOR('',#4256,0.31);
#1330=VECTOR('',#4261,0.3);
#1331=VECTOR('',#4266,0.27);
#1332=VECTOR('',#4271,1.);
#1333=VECTOR('',#4272,1.);
#1334=VECTOR('',#4273,1.);
#1335=VECTOR('',#4274,1.);
#1336=VECTOR('',#4277,1.);
#1337=VECTOR('',#4278,1.);
#1338=VECTOR('',#4279,1.);
#1339=VECTOR('',#4282,1.);
#1340=VECTOR('',#4283,1.);
#1341=VECTOR('',#4284,1.);
#1342=VECTOR('',#4287,1.);
#1343=VECTOR('',#4288,1.);
#1344=VECTOR('',#4289,1.);
#1345=VECTOR('',#4292,1.);
#1346=VECTOR('',#4293,1.);
#1347=VECTOR('',#4294,1.);
#1348=VECTOR('',#4297,1.);
#1349=VECTOR('',#4298,1.);
#1587=VERTEX_POINT('',#5195);
#1588=VERTEX_POINT('',#5198);
#1589=VERTEX_POINT('',#5202);
#1590=VERTEX_POINT('',#5206);
#1591=VERTEX_POINT('',#5210);
#1592=VERTEX_POINT('',#5213);
#1593=VERTEX_POINT('',#5217);
#1594=VERTEX_POINT('',#5221);
#1595=VERTEX_POINT('',#5226);
#1596=VERTEX_POINT('',#5227);
#1597=VERTEX_POINT('',#5229);
#1598=VERTEX_POINT('',#5231);
#1599=VERTEX_POINT('',#5235);
#1600=VERTEX_POINT('',#5237);
#1601=VERTEX_POINT('',#5241);
#1602=VERTEX_POINT('',#5243);
#1603=VERTEX_POINT('',#5247);
#1604=VERTEX_POINT('',#5249);
#1605=VERTEX_POINT('',#5253);
#1606=VERTEX_POINT('',#5255);
#1934=EDGE_CURVE('',#1587,#1587,#330,.T.);
#1935=EDGE_CURVE('',#1588,#1588,#331,.T.);
#1936=EDGE_CURVE('',#1588,#1587,#1053,.T.);
#1937=EDGE_CURVE('',#1589,#1589,#332,.T.);
#1938=EDGE_CURVE('',#1589,#1588,#1054,.T.);
#1939=EDGE_CURVE('',#1590,#1590,#333,.T.);
#1940=EDGE_CURVE('',#1590,#1589,#1055,.T.);
#1941=EDGE_CURVE('',#1591,#1591,#334,.T.);
#1942=EDGE_CURVE('',#1592,#1592,#335,.F.);
#1943=EDGE_CURVE('',#1592,#1591,#1056,.T.);
#1944=EDGE_CURVE('',#1593,#1593,#336,.F.);
#1945=EDGE_CURVE('',#1593,#1592,#1057,.T.);
#1946=EDGE_CURVE('',#1594,#1594,#337,.T.);
#1947=EDGE_CURVE('',#1594,#1593,#1058,.T.);
#1948=EDGE_CURVE('',#1595,#1596,#1059,.T.);
#1949=EDGE_CURVE('',#1596,#1597,#1060,.T.);
#1950=EDGE_CURVE('',#1597,#1598,#1061,.T.);
#1951=EDGE_CURVE('',#1595,#1598,#1062,.T.);
#1952=EDGE_CURVE('',#1596,#1599,#1063,.T.);
#1953=EDGE_CURVE('',#1599,#1600,#1064,.T.);
#1954=EDGE_CURVE('',#1600,#1597,#1065,.T.);
#1955=EDGE_CURVE('',#1599,#1601,#1066,.T.);
#1956=EDGE_CURVE('',#1601,#1602,#1067,.T.);
#1957=EDGE_CURVE('',#1602,#1600,#1068,.T.);
#1958=EDGE_CURVE('',#1601,#1603,#1069,.T.);
#1959=EDGE_CURVE('',#1603,#1604,#1070,.T.);
#1960=EDGE_CURVE('',#1604,#1602,#1071,.T.);
#1961=EDGE_CURVE('',#1603,#1605,#1072,.T.);
#1962=EDGE_CURVE('',#1605,#1606,#1073,.T.);
#1963=EDGE_CURVE('',#1606,#1604,#1074,.T.);
#1964=EDGE_CURVE('',#1605,#1595,#1075,.T.);
#1965=EDGE_CURVE('',#1598,#1606,#1076,.T.);
#2568=ORIENTED_EDGE('',*,*,#1934,.F.);
#2569=ORIENTED_EDGE('',*,*,#1935,.F.);
#2570=ORIENTED_EDGE('',*,*,#1936,.T.);
#2571=ORIENTED_EDGE('',*,*,#1934,.T.);
#2572=ORIENTED_EDGE('',*,*,#1936,.F.);
#2573=ORIENTED_EDGE('',*,*,#1937,.F.);
#2574=ORIENTED_EDGE('',*,*,#1938,.T.);
#2575=ORIENTED_EDGE('',*,*,#1935,.T.);
#2576=ORIENTED_EDGE('',*,*,#1938,.F.);
#2577=ORIENTED_EDGE('',*,*,#1939,.F.);
#2578=ORIENTED_EDGE('',*,*,#1940,.T.);
#2579=ORIENTED_EDGE('',*,*,#1937,.T.);
#2580=ORIENTED_EDGE('',*,*,#1940,.F.);
#2581=ORIENTED_EDGE('',*,*,#1939,.T.);
#2582=ORIENTED_EDGE('',*,*,#1941,.F.);
#2583=ORIENTED_EDGE('',*,*,#1942,.F.);
#2584=ORIENTED_EDGE('',*,*,#1943,.T.);
#2585=ORIENTED_EDGE('',*,*,#1941,.T.);
#2586=ORIENTED_EDGE('',*,*,#1943,.F.);
#2587=ORIENTED_EDGE('',*,*,#1944,.F.);
#2588=ORIENTED_EDGE('',*,*,#1945,.T.);
#2589=ORIENTED_EDGE('',*,*,#1942,.T.);
#2590=ORIENTED_EDGE('',*,*,#1945,.F.);
#2591=ORIENTED_EDGE('',*,*,#1946,.F.);
#2592=ORIENTED_EDGE('',*,*,#1947,.T.);
#2593=ORIENTED_EDGE('',*,*,#1944,.T.);
#2594=ORIENTED_EDGE('',*,*,#1947,.F.);
#2595=ORIENTED_EDGE('',*,*,#1946,.T.);
#2596=ORIENTED_EDGE('',*,*,#1948,.T.);
#2597=ORIENTED_EDGE('',*,*,#1949,.T.);
#2598=ORIENTED_EDGE('',*,*,#1950,.T.);
#2599=ORIENTED_EDGE('',*,*,#1951,.F.);
#2600=ORIENTED_EDGE('',*,*,#1952,.T.);
#2601=ORIENTED_EDGE('',*,*,#1953,.T.);
#2602=ORIENTED_EDGE('',*,*,#1954,.T.);
#2603=ORIENTED_EDGE('',*,*,#1949,.F.);
#2604=ORIENTED_EDGE('',*,*,#1955,.T.);
#2605=ORIENTED_EDGE('',*,*,#1956,.T.);
#2606=ORIENTED_EDGE('',*,*,#1957,.T.);
#2607=ORIENTED_EDGE('',*,*,#1953,.F.);
#2608=ORIENTED_EDGE('',*,*,#1958,.T.);
#2609=ORIENTED_EDGE('',*,*,#1959,.T.);
#2610=ORIENTED_EDGE('',*,*,#1960,.T.);
#2611=ORIENTED_EDGE('',*,*,#1956,.F.);
#2612=ORIENTED_EDGE('',*,*,#1961,.T.);
#2613=ORIENTED_EDGE('',*,*,#1962,.T.);
#2614=ORIENTED_EDGE('',*,*,#1963,.T.);
#2615=ORIENTED_EDGE('',*,*,#1959,.F.);
#2616=ORIENTED_EDGE('',*,*,#1964,.T.);
#2617=ORIENTED_EDGE('',*,*,#1951,.T.);
#2618=ORIENTED_EDGE('',*,*,#1965,.T.);
#2619=ORIENTED_EDGE('',*,*,#1962,.F.);
#2620=ORIENTED_EDGE('',*,*,#1964,.F.);
#2621=ORIENTED_EDGE('',*,*,#1961,.F.);
#2622=ORIENTED_EDGE('',*,*,#1958,.F.);
#2623=ORIENTED_EDGE('',*,*,#1955,.F.);
#2624=ORIENTED_EDGE('',*,*,#1952,.F.);
#2625=ORIENTED_EDGE('',*,*,#1948,.F.);
#2626=ORIENTED_EDGE('',*,*,#1965,.F.);
#2627=ORIENTED_EDGE('',*,*,#1950,.F.);
#2628=ORIENTED_EDGE('',*,*,#1954,.F.);
#2629=ORIENTED_EDGE('',*,*,#1957,.F.);
#2630=ORIENTED_EDGE('',*,*,#1960,.F.);
#2631=ORIENTED_EDGE('',*,*,#1963,.F.);
#3020=PLANE('',#3566);
#3021=PLANE('',#3574);
#3022=PLANE('',#3582);
#3023=PLANE('',#3583);
#3024=PLANE('',#3584);
#3025=PLANE('',#3585);
#3026=PLANE('',#3586);
#3027=PLANE('',#3587);
#3028=PLANE('',#3588);
#3029=PLANE('',#3589);
#3030=PLANE('',#3590);
#3165=ADVANCED_FACE('',(#544),#3020,.T.);
#3166=ADVANCED_FACE('',(#545),#129,.T.);
#3167=ADVANCED_FACE('',(#546),#428,.T.);
#3168=ADVANCED_FACE('',(#547),#130,.T.);
#3169=ADVANCED_FACE('',(#548,#249),#3021,.T.);
#3170=ADVANCED_FACE('',(#549),#131,.T.);
#3171=ADVANCED_FACE('',(#550),#429,.T.);
#3172=ADVANCED_FACE('',(#551),#132,.T.);
#3173=ADVANCED_FACE('',(#552),#3022,.T.);
#3174=ADVANCED_FACE('',(#553),#3023,.F.);
#3175=ADVANCED_FACE('',(#554),#3024,.F.);
#3176=ADVANCED_FACE('',(#555),#3025,.F.);
#3177=ADVANCED_FACE('',(#556),#3026,.F.);
#3178=ADVANCED_FACE('',(#557),#3027,.F.);
#3179=ADVANCED_FACE('',(#558),#3028,.F.);
#3180=ADVANCED_FACE('',(#559),#3029,.F.);
#3181=ADVANCED_FACE('',(#560),#3030,.F.);
#3266=CLOSED_SHELL('',(#3165,#3166,#3167,#3168,#3169,#3170,#3171,#3172,
#3173));
#3267=CLOSED_SHELL('',(#3174,#3175,#3176,#3177,#3178,#3179,#3180,#3181));
#3565=AXIS2_PLACEMENT_3D('',#5193,#4227,#4228);
#3566=AXIS2_PLACEMENT_3D('',#5194,#4229,#4230);
#3567=AXIS2_PLACEMENT_3D('',#5196,#4231,#4232);
#3568=AXIS2_PLACEMENT_3D('',#5197,#4233,#4234);
#3569=AXIS2_PLACEMENT_3D('',#5199,#4235,#4236);
#3570=AXIS2_PLACEMENT_3D('',#5201,#4238,#4239);
#3571=AXIS2_PLACEMENT_3D('',#5203,#4240,#4241);
#3572=AXIS2_PLACEMENT_3D('',#5205,#4243,#4244);
#3573=AXIS2_PLACEMENT_3D('',#5207,#4245,#4246);
#3574=AXIS2_PLACEMENT_3D('',#5209,#4248,#4249);
#3575=AXIS2_PLACEMENT_3D('',#5211,#4250,#4251);
#3576=AXIS2_PLACEMENT_3D('',#5212,#4252,#4253);
#3577=AXIS2_PLACEMENT_3D('',#5214,#4254,#4255);
#3578=AXIS2_PLACEMENT_3D('',#5216,#4257,#4258);
#3579=AXIS2_PLACEMENT_3D('',#5218,#4259,#4260);
#3580=AXIS2_PLACEMENT_3D('',#5220,#4262,#4263);
#3581=AXIS2_PLACEMENT_3D('',#5222,#4264,#4265);
#3582=AXIS2_PLACEMENT_3D('',#5224,#4267,#4268);
#3583=AXIS2_PLACEMENT_3D('',#5225,#4269,#4270);
#3584=AXIS2_PLACEMENT_3D('',#5234,#4275,#4276);
#3585=AXIS2_PLACEMENT_3D('',#5240,#4280,#4281);
#3586=AXIS2_PLACEMENT_3D('',#5246,#4285,#4286);
#3587=AXIS2_PLACEMENT_3D('',#5252,#4290,#4291);
#3588=AXIS2_PLACEMENT_3D('',#5258,#4295,#4296);
#3589=AXIS2_PLACEMENT_3D('',#5261,#4299,#4300);
#3590=AXIS2_PLACEMENT_3D('',#5262,#4301,#4302);
#4227=DIRECTION('axis',(0.,0.,1.));
#4228=DIRECTION('refdir',(1.,0.,0.));
#4229=DIRECTION('center_axis',(0.,1.,0.));
#4230=DIRECTION('ref_axis',(0.,0.,1.));
#4231=DIRECTION('center_axis',(0.,-1.,0.));
#4232=DIRECTION('ref_axis',(1.,0.,0.));
#4233=DIRECTION('center_axis',(0.,-1.,0.));
#4234=DIRECTION('ref_axis',(1.,0.,0.));
#4235=DIRECTION('center_axis',(0.,-1.,0.));
#4236=DIRECTION('ref_axis',(1.,0.,0.));
#4237=DIRECTION('',(0.707106781186548,0.707106781186547,8.65956056235494E-17));
#4238=DIRECTION('center_axis',(0.,-1.,0.));
#4239=DIRECTION('ref_axis',(1.,0.,0.));
#4240=DIRECTION('center_axis',(0.,-1.,0.));
#4241=DIRECTION('ref_axis',(1.,0.,0.));
#4242=DIRECTION('',(0.,1.,0.));
#4243=DIRECTION('center_axis',(0.,1.,0.));
#4244=DIRECTION('ref_axis',(1.,0.,0.));
#4245=DIRECTION('center_axis',(0.,-1.,0.));
#4246=DIRECTION('ref_axis',(1.,0.,0.));
#4247=DIRECTION('',(-0.707106781186547,0.707106781186548,-8.65956056235493E-17));
#4248=DIRECTION('center_axis',(0.,-1.,0.));
#4249=DIRECTION('ref_axis',(0.,0.,-1.));
#4250=DIRECTION('center_axis',(0.,-1.,0.));
#4251=DIRECTION('ref_axis',(1.,0.,0.));
#4252=DIRECTION('center_axis',(0.,1.,0.));
#4253=DIRECTION('ref_axis',(1.,0.,0.));
#4254=DIRECTION('center_axis',(0.,1.,0.));
#4255=DIRECTION('ref_axis',(1.,0.,0.));
#4256=DIRECTION('',(-0.447213595499958,0.894427190999916,-5.47678698264203E-17));
#4257=DIRECTION('center_axis',(0.,-1.,0.));
#4258=DIRECTION('ref_axis',(1.,0.,0.));
#4259=DIRECTION('center_axis',(0.,1.,0.));
#4260=DIRECTION('ref_axis',(1.,0.,0.));
#4261=DIRECTION('',(0.,1.,0.));
#4262=DIRECTION('center_axis',(0.,1.,0.));
#4263=DIRECTION('ref_axis',(1.,0.,0.));
#4264=DIRECTION('center_axis',(0.,-1.,0.));
#4265=DIRECTION('ref_axis',(1.,0.,0.));
#4266=DIRECTION('',(-0.707106781186547,0.707106781186548,-8.65956056235493E-17));
#4267=DIRECTION('center_axis',(0.,-1.,0.));
#4268=DIRECTION('ref_axis',(0.,0.,-1.));
#4269=DIRECTION('center_axis',(0.866025403784439,0.,-0.5));
#4270=DIRECTION('ref_axis',(0.5,0.,0.866025403784439));
#4271=DIRECTION('',(-0.5,0.,-0.866025403784439));
#4272=DIRECTION('',(0.,-1.,0.));
#4273=DIRECTION('',(0.5,0.,0.866025403784439));
#4274=DIRECTION('',(0.,-1.,0.));
#4275=DIRECTION('center_axis',(1.92296268638356E-16,0.,-1.));
#4276=DIRECTION('ref_axis',(1.,0.,1.92296268638356E-16));
#4277=DIRECTION('',(-1.,0.,-1.92296268638356E-16));
#4278=DIRECTION('',(0.,-1.,0.));
#4279=DIRECTION('',(1.,0.,1.92296268638356E-16));
#4280=DIRECTION('center_axis',(-0.866025403784439,0.,-0.5));
#4281=DIRECTION('ref_axis',(0.5,0.,-0.866025403784439));
#4282=DIRECTION('',(-0.5,0.,0.866025403784438));
#4283=DIRECTION('',(0.,-1.,0.));
#4284=DIRECTION('',(0.5,0.,-0.866025403784438));
#4285=DIRECTION('center_axis',(-0.866025403784439,0.,0.5));
#4286=DIRECTION('ref_axis',(-0.5,0.,-0.866025403784439));
#4287=DIRECTION('',(0.5,0.,0.866025403784439));
#4288=DIRECTION('',(0.,-1.,0.));
#4289=DIRECTION('',(-0.5,0.,-0.866025403784439));
#4290=DIRECTION('center_axis',(-1.92296268638356E-16,0.,1.));
#4291=DIRECTION('ref_axis',(-1.,0.,-1.92296268638356E-16));
#4292=DIRECTION('',(1.,0.,1.92296268638356E-16));
#4293=DIRECTION('',(0.,-1.,0.));
#4294=DIRECTION('',(-1.,0.,-1.92296268638356E-16));
#4295=DIRECTION('center_axis',(0.866025403784439,0.,0.5));
#4296=DIRECTION('ref_axis',(-0.5,0.,0.866025403784439));
#4297=DIRECTION('',(0.5,0.,-0.866025403784439));
#4298=DIRECTION('',(-0.5,0.,0.866025403784439));
#4299=DIRECTION('center_axis',(0.,1.,0.));
#4300=DIRECTION('ref_axis',(1.,0.,0.));
#4301=DIRECTION('center_axis',(0.,-1.,0.));
#4302=DIRECTION('ref_axis',(0.,0.,-1.));
#5193=CARTESIAN_POINT('',(0.,0.,0.));
#5194=CARTESIAN_POINT('Origin',(0.45,0.6,0.));
#5195=CARTESIAN_POINT('',(-0.45,0.6,-5.51091059616309E-17));
#5196=CARTESIAN_POINT('Origin',(0.,0.6,0.));
#5197=CARTESIAN_POINT('Origin',(0.,0.575,0.));
#5198=CARTESIAN_POINT('',(-0.5,0.55,-6.12323399573677E-17));
#5199=CARTESIAN_POINT('Origin',(0.,0.55,0.));
#5200=CARTESIAN_POINT('',(-0.475,0.575,-5.81707229594993E-17));
#5201=CARTESIAN_POINT('Origin',(0.,0.29,0.));
#5202=CARTESIAN_POINT('',(-0.5,0.0299999999999998,-6.12323399573677E-17));
#5203=CARTESIAN_POINT('Origin',(0.,0.0299999999999998,0.));
#5204=CARTESIAN_POINT('',(-0.5,0.29,-6.12323399573677E-17));
#5205=CARTESIAN_POINT('Origin',(0.,0.0150000000000001,0.));
#5206=CARTESIAN_POINT('',(-0.47,7.11236625150491E-17,-5.75583995599256E-17));
#5207=CARTESIAN_POINT('Origin',(0.,0.,0.));
#5208=CARTESIAN_POINT('',(-0.485,0.0150000000000001,-5.93953697586466E-17));
#5209=CARTESIAN_POINT('Origin',(0.32,0.,0.));
#5210=CARTESIAN_POINT('',(-0.32,-6.93889390390723E-18,-3.91886975727153E-17));
#5211=CARTESIAN_POINT('Origin',(0.,0.,0.));
#5212=CARTESIAN_POINT('Origin',(0.,-0.02,0.));
#5213=CARTESIAN_POINT('',(-0.2942,-0.0515999999999999,3.60291088309151E-17));
#5214=CARTESIAN_POINT('Origin',(0.,-0.0515999999999999,0.));
#5215=CARTESIAN_POINT('',(-0.31,-0.02,-3.7964050773568E-17));
#5216=CARTESIAN_POINT('Origin',(0.,-1.24,0.));
#5217=CARTESIAN_POINT('',(-0.2942,-2.4458,3.60291088309151E-17));
#5218=CARTESIAN_POINT('Origin',(0.,-2.4458,0.));
#5219=CARTESIAN_POINT('',(-0.2942,-1.24,-3.60291088309151E-17));
#5220=CARTESIAN_POINT('Origin',(0.,-2.47,0.));
#5221=CARTESIAN_POINT('',(-0.24,-2.5,-2.93915231795365E-17));
#5222=CARTESIAN_POINT('Origin',(0.,-2.5,0.));
#5223=CARTESIAN_POINT('',(-0.27,-2.47,-3.30654635769785E-17));
#5224=CARTESIAN_POINT('Origin',(0.,-2.5,0.));
#5225=CARTESIAN_POINT('Origin',(0.144337567297406,-0.6,-0.25));
#5226=CARTESIAN_POINT('',(0.288675134594813,-0.6,0.));
#5227=CARTESIAN_POINT('',(0.144337567297406,-0.6,-0.25));
#5228=CARTESIAN_POINT('',(0.288675134594813,-0.6,0.));
#5229=CARTESIAN_POINT('',(0.144337567297406,-0.96,-0.25));
#5230=CARTESIAN_POINT('',(0.144337567297406,-0.6,-0.25));
#5231=CARTESIAN_POINT('',(0.288675134594813,-0.96,0.));
#5232=CARTESIAN_POINT('',(0.288675134594813,-0.96,0.));
#5233=CARTESIAN_POINT('',(0.288675134594813,-0.6,0.));
#5234=CARTESIAN_POINT('Origin',(-0.144337567297406,-0.6,-0.25));
#5235=CARTESIAN_POINT('',(-0.144337567297406,-0.6,-0.25));
#5236=CARTESIAN_POINT('',(0.144337567297406,-0.6,-0.25));
#5237=CARTESIAN_POINT('',(-0.144337567297406,-0.96,-0.25));
#5238=CARTESIAN_POINT('',(-0.144337567297406,-0.6,-0.25));
#5239=CARTESIAN_POINT('',(0.144337567297406,-0.96,-0.25));
#5240=CARTESIAN_POINT('Origin',(-0.288675134594813,-0.6,-8.32667268468867E-17));
#5241=CARTESIAN_POINT('',(-0.288675134594813,-0.6,-3.53525079574969E-17));
#5242=CARTESIAN_POINT('',(-0.144337567297406,-0.6,-0.25));
#5243=CARTESIAN_POINT('',(-0.288675134594813,-0.96,-5.55111512312578E-17));
#5244=CARTESIAN_POINT('',(-0.288675134594813,-0.6,-3.53525079574969E-17));
#5245=CARTESIAN_POINT('',(-0.144337567297406,-0.96,-0.25));
#5246=CARTESIAN_POINT('Origin',(-0.144337567297407,-0.6,0.25));
#5247=CARTESIAN_POINT('',(-0.144337567297407,-0.6,0.25));
#5248=CARTESIAN_POINT('',(-0.288675134594813,-0.6,-3.53525079574969E-17));
#5249=CARTESIAN_POINT('',(-0.144337567297407,-0.96,0.25));
#5250=CARTESIAN_POINT('',(-0.144337567297407,-0.6,0.25));
#5251=CARTESIAN_POINT('',(-0.288675134594813,-0.96,-3.53525079574969E-17));
#5252=CARTESIAN_POINT('Origin',(0.144337567297406,-0.6,0.25));
#5253=CARTESIAN_POINT('',(0.144337567297406,-0.6,0.25));
#5254=CARTESIAN_POINT('',(-0.144337567297407,-0.6,0.25));
#5255=CARTESIAN_POINT('',(0.144337567297406,-0.96,0.25));
#5256=CARTESIAN_POINT('',(0.144337567297406,-0.6,0.25));
#5257=CARTESIAN_POINT('',(-0.144337567297407,-0.96,0.25));
#5258=CARTESIAN_POINT('Origin',(0.288675134594813,-0.6,0.));
#5259=CARTESIAN_POINT('',(0.144337567297406,-0.6,0.25));
#5260=CARTESIAN_POINT('',(0.144337567297406,-0.96,0.25));
#5261=CARTESIAN_POINT('Origin',(0.,-0.6,0.));
#5262=CARTESIAN_POINT('Origin',(0.,-0.96,0.));
#5679=UNCERTAINTY_MEASURE_WITH_UNIT(LENGTH_MEASURE(0.001),#5703,
'DISTANCE_ACCURACY_VALUE',
'Maximum model space distance between geometric entities at asserted c
onnectivities');
#5688=UNCERTAINTY_MEASURE_WITH_UNIT(LENGTH_MEASURE(0.001),#5703,
'DISTANCE_ACCURACY_VALUE',
'Maximum model space distance between geometric entities at asserted c
onnectivities');
#5693=(
GEOMETRIC_REPRESENTATION_CONTEXT(3)
GLOBAL_UNCERTAINTY_ASSIGNED_CONTEXT((#5679))
GLOBAL_UNIT_ASSIGNED_CONTEXT((#5703,#5705,#5706))
REPRESENTATION_CONTEXT('','3D')
);
#5702=(
GEOMETRIC_REPRESENTATION_CONTEXT(3)
GLOBAL_UNCERTAINTY_ASSIGNED_CONTEXT((#5688))
GLOBAL_UNIT_ASSIGNED_CONTEXT((#5703,#5705,#5706))
REPRESENTATION_CONTEXT('','3D')
);
#5703=(
LENGTH_UNIT()
NAMED_UNIT(*)
SI_UNIT(.CENTI.,.METRE.)
);
#5705=(
NAMED_UNIT(*)
PLANE_ANGLE_UNIT()
SI_UNIT($,.RADIAN.)
);
#5706=(
NAMED_UNIT(*)
SI_UNIT($,.STERADIAN.)
SOLID_ANGLE_UNIT()
);
#5711=SHAPE_DEFINITION_REPRESENTATION(#5724,#5763);
#5724=PRODUCT_DEFINITION_SHAPE('',$,#5777);
#5763=SHAPE_REPRESENTATION('',(#3565),#5693);
#5772=PRODUCT_DEFINITION_CONTEXT('part definition',#5813,'design');
#5777=PRODUCT_DEFINITION('Cap Screw - M6x25','Cap Screw - M6x25',
#5790,#5772);
#5790=PRODUCT_DEFINITION_FORMATION('',$,#5819);
#5813=APPLICATION_CONTEXT(
'Core Data for Automotive Mechanical Design Process');
#5814=PRODUCT_CONTEXT('part definition',#5813,'mechanical');
#5819=PRODUCT('Cap Screw - M6x25','Cap Screw - M6x25',
'Cap Screw - M6x25',(#5814));
#5898=COLOUR_RGB('Black',0.12,0.14,0.17);
#5899=FILL_AREA_STYLE_COLOUR('',#5898);
#5900=FILL_AREA_STYLE('',(#5899));
#5901=SURFACE_STYLE_FILL_AREA(#5900);
#5902=SURFACE_SIDE_STYLE('',(#5901));
#5903=SURFACE_STYLE_USAGE(.BOTH.,#5902);
#5904=PRESENTATION_STYLE_ASSIGNMENT((#5903));
ENDSEC;
END-ISO-10303-21;
